ISO-10303-21;
HEADER;
/* Generated by software containing ST-Developer
 * from STEP Tools, Inc. (www.steptools.com) 
 */

FILE_DESCRIPTION(
/* description */ ('Belt conveyor head drive unit'),
/* implementation_level */ '2;1');

FILE_NAME(
/* name */ 'M4 clamp nut (2).step',
/* time_stamp */ '2026-10-28T03:26:19-07:00',
/* author */ (''),
/* organization */ (''),
/* preprocessor_version */ 'ST-DEVELOPER v20.2',
/* originating_system */ 'Autodesk Translation Framework v15.17.0.0',
/* authorisation */ '');

FILE_SCHEMA (('AUTOMOTIVE_DESIGN { 1 0 10303 214 3 1 1 }'));
ENDSEC;

DATA;
#10=MECHANICAL_DESIGN_GEOMETRIC_PRESENTATION_REPRESENTATION('',(#857),#27069);
#719=SHAPE_REPRESENTATION_RELATIONSHIP('SRR','None',#27363,#788);
#788=ADVANCED_BREP_SHAPE_REPRESENTATION('',(#942),#27005);
#857=STYLED_ITEM('',(#27804),#942);
#942=MANIFOLD_SOLID_BREP('Body1',#13722);
#1080=FACE_BOUND('',#2648,.T.);
#1081=FACE_BOUND('',#2650,.T.);
#1352=PLANE('',#14867);
#1353=PLANE('',#14868);
#1777=FACE_OUTER_BOUND('',#2645,.T.);
#1778=FACE_OUTER_BOUND('',#2646,.T.);
#1779=FACE_OUTER_BOUND('',#2647,.T.);
#1780=FACE_OUTER_BOUND('',#2649,.T.);
#2645=EDGE_LOOP('',(#9618,#9619,#9620,#9621));
#2646=EDGE_LOOP('',(#9622,#9623,#9624,#9625));
#2647=EDGE_LOOP('',(#9626));
#2648=EDGE_LOOP('',(#9627));
#2649=EDGE_LOOP('',(#9628));
#2650=EDGE_LOOP('',(#9629));
#3686=LINE('',#21681,#4478);
#3687=LINE('',#21687,#4479);
#4478=VECTOR('',#17224,0.164999999999999);
#4479=VECTOR('',#17231,0.4);
#5224=CIRCLE('',#14862,0.164999999999999);
#5225=CIRCLE('',#14863,0.164999999999999);
#5226=CIRCLE('',#14865,0.4);
#5227=CIRCLE('',#14866,0.4);
#6173=VERTEX_POINT('',#21678);
#6174=VERTEX_POINT('',#21680);
#6175=VERTEX_POINT('',#21684);
#6176=VERTEX_POINT('',#21686);
#7501=EDGE_CURVE('',#6173,#6173,#5224,.T.);
#7502=EDGE_CURVE('',#6173,#6174,#3686,.T.);
#7503=EDGE_CURVE('',#6174,#6174,#5225,.T.);
#7504=EDGE_CURVE('',#6175,#6175,#5226,.T.);
#7505=EDGE_CURVE('',#6175,#6176,#3687,.T.);
#7506=EDGE_CURVE('',#6176,#6176,#5227,.T.);
#9618=ORIENTED_EDGE('',*,*,#7501,.F.);
#9619=ORIENTED_EDGE('',*,*,#7502,.T.);
#9620=ORIENTED_EDGE('',*,*,#7503,.T.);
#9621=ORIENTED_EDGE('',*,*,#7502,.F.);
#9622=ORIENTED_EDGE('',*,*,#7504,.F.);
#9623=ORIENTED_EDGE('',*,*,#7505,.T.);
#9624=ORIENTED_EDGE('',*,*,#7506,.T.);
#9625=ORIENTED_EDGE('',*,*,#7505,.F.);
#9626=ORIENTED_EDGE('',*,*,#7504,.T.);
#9627=ORIENTED_EDGE('',*,*,#7501,.T.);
#9628=ORIENTED_EDGE('',*,*,#7506,.F.);
#9629=ORIENTED_EDGE('',*,*,#7503,.F.);
#12601=CYLINDRICAL_SURFACE('',#14861,0.164999999999999);
#12602=CYLINDRICAL_SURFACE('',#14864,0.4);
#13056=ADVANCED_FACE('',(#1777),#12601,.F.);
#13057=ADVANCED_FACE('',(#1778),#12602,.T.);
#13058=ADVANCED_FACE('',(#1779,#1080),#1352,.T.);
#13059=ADVANCED_FACE('',(#1780,#1081),#1353,.F.);
#13722=CLOSED_SHELL('',(#13056,#13057,#13058,#13059));
#14860=AXIS2_PLACEMENT_3D('',#21676,#17218,#17219);
#14861=AXIS2_PLACEMENT_3D('',#21677,#17220,#17221);
#14862=AXIS2_PLACEMENT_3D('',#21679,#17222,#17223);
#14863=AXIS2_PLACEMENT_3D('',#21682,#17225,#17226);
#14864=AXIS2_PLACEMENT_3D('',#21683,#17227,#17228);
#14865=AXIS2_PLACEMENT_3D('',#21685,#17229,#17230);
#14866=AXIS2_PLACEMENT_3D('',#21688,#17232,#17233);
#14867=AXIS2_PLACEMENT_3D('',#21689,#17234,#17235);
#14868=AXIS2_PLACEMENT_3D('',#21690,#17236,#17237);
#17218=DIRECTION('axis',(0.,0.,1.));
#17219=DIRECTION('refdir',(1.,0.,0.));
#17220=DIRECTION('center_axis',(0.,0.,1.));
#17221=DIRECTION('ref_axis',(1.,0.,0.));
#17222=DIRECTION('center_axis',(0.,0.,-1.));
#17223=DIRECTION('ref_axis',(1.,0.,0.));
#17224=DIRECTION('',(0.,0.,-1.));
#17225=DIRECTION('center_axis',(0.,0.,-1.));
#17226=DIRECTION('ref_axis',(1.,0.,0.));
#17227=DIRECTION('center_axis',(0.,0.,1.));
#17228=DIRECTION('ref_axis',(1.,0.,0.));
#17229=DIRECTION('center_axis',(0.,0.,1.));
#17230=DIRECTION('ref_axis',(1.,0.,0.));
#17231=DIRECTION('',(0.,0.,-1.));
#17232=DIRECTION('center_axis',(0.,0.,1.));
#17233=DIRECTION('ref_axis',(1.,0.,0.));
#17234=DIRECTION('center_axis',(0.,0.,1.));
#17235=DIRECTION('ref_axis',(1.,0.,0.));
#17236=DIRECTION('center_axis',(0.,0.,1.));
#17237=DIRECTION('ref_axis',(1.,0.,0.));
#21676=CARTESIAN_POINT('',(0.,0.,0.));
#21677=CARTESIAN_POINT('Origin',(9.77091003018116,-1.,-1.6));
#21678=CARTESIAN_POINT('',(9.60591003018116,-1.,-1.2));
#21679=CARTESIAN_POINT('Origin',(9.77091003018116,-1.,-1.2));
#21680=CARTESIAN_POINT('',(9.60591003018116,-1.,-1.6));
#21681=CARTESIAN_POINT('',(9.60591003018116,-1.,-1.6));
#21682=CARTESIAN_POINT('Origin',(9.77091003018116,-1.,-1.6));
#21683=CARTESIAN_POINT('Origin',(9.77091003018116,-1.,-1.6));
#21684=CARTESIAN_POINT('',(9.37091003018116,-1.,-1.2));
#21685=CARTESIAN_POINT('Origin',(9.77091003018116,-1.,-1.2));
#21686=CARTESIAN_POINT('',(9.37091003018116,-1.,-1.6));
#21687=CARTESIAN_POINT('',(9.37091003018116,-1.,-1.6));
#21688=CARTESIAN_POINT('Origin',(9.77091003018116,-1.,-1.6));
#21689=CARTESIAN_POINT('Origin',(9.77091003018116,-1.,-1.2));
#21690=CARTESIAN_POINT('Origin',(9.77091003018116,-1.,-1.6));
#26928=UNCERTAINTY_MEASURE_WITH_UNIT(LENGTH_MEASURE(0.001),#27070,
'DISTANCE_ACCURACY_VALUE',
'Maximum model space distance between geometric entities at asserted c
onnectivities');
#26992=UNCERTAINTY_MEASURE_WITH_UNIT(LENGTH_MEASURE(0.001),#27070,
'DISTANCE_ACCURACY_VALUE',
'Maximum model space distance between geometric entities at asserted c
onnectivities');
#27005=(
GEOMETRIC_REPRESENTATION_CONTEXT(3)
GLOBAL_UNCERTAINTY_ASSIGNED_CONTEXT((#26928))
GLOBAL_UNIT_ASSIGNED_CONTEXT((#27070,#27072,#27073))
REPRESENTATION_CONTEXT('','3D')
);
#27069=(
GEOMETRIC_REPRESENTATION_CONTEXT(3)
GLOBAL_UNCERTAINTY_ASSIGNED_CONTEXT((#26992))
GLOBAL_UNIT_ASSIGNED_CONTEXT((#27070,#27072,#27073))
REPRESENTATION_CONTEXT('','3D')
);
#27070=(
LENGTH_UNIT()
NAMED_UNIT(*)
SI_UNIT(.CENTI.,.METRE.)
);
#27072=(
NAMED_UNIT(*)
PLANE_ANGLE_UNIT()
SI_UNIT($,.RADIAN.)
);
#27073=(
NAMED_UNIT(*)
SI_UNIT($,.STERADIAN.)
SOLID_ANGLE_UNIT()
);
#27086=SHAPE_DEFINITION_REPRESENTATION(#27162,#27363);
#27162=PRODUCT_DEFINITION_SHAPE('',$,#27440);
#27363=SHAPE_REPRESENTATION('',(#14860),#27005);
#27427=PRODUCT_DEFINITION_CONTEXT('part definition',#27657,'design');
#27440=PRODUCT_DEFINITION('M4 clamp nut (2)','M4 clamp nut (2)',#27516,#27427);
#27516=PRODUCT_DEFINITION_FORMATION('',$,#27671);
#27657=APPLICATION_CONTEXT(
'Core Data for Automotive Mechanical Design Process');
#27658=PRODUCT_CONTEXT('part definition',#27657,'mechanical');
#27671=PRODUCT('M4 clamp nut (2)','M4 clamp nut (2)','M4 clamp nut (2)',(#27658));
#27798=COLOUR_RGB('Black',0.12,0.14,0.17);
#27799=FILL_AREA_STYLE_COLOUR('',#27798);
#27800=FILL_AREA_STYLE('',(#27799));
#27801=SURFACE_STYLE_FILL_AREA(#27800);
#27802=SURFACE_SIDE_STYLE('',(#27801));
#27803=SURFACE_STYLE_USAGE(.BOTH.,#27802);
#27804=PRESENTATION_STYLE_ASSIGNMENT((#27803));
ENDSEC;
END-ISO-10303-21;
